ISO-10303-21;
HEADER;
FILE_DESCRIPTION (('STEP AP214'),
    '1' );
FILE_NAME ('Servo-Axe.step',
    '2026-11-01T05:08:46',
    ( '' ),
    ( '' ),
    'SwSTEP 2.0',
    'SolidWorks 2024',
    '' );
FILE_SCHEMA (( 'AUTOMOTIVE_DESIGN' ));
ENDSEC;

DATA;
#8=CARTESIAN_POINT ( 'NONE',  ( 0.000000000000000000, 10.00000000000000000, 0.000000000000000000 ) ) ;
#12=CIRCLE ( 'NONE', #9067, 0.9999999999999950040 ) ;
#45=ADVANCED_FACE ( 'NONE', ( #6580 ), #11842, .F. ) ;
#214=VERTEX_POINT ( 'NONE', #8661 ) ;
#218=DIRECTION ( 'NONE',  ( -0.000000000000000000, 1.000000000000000000, -0.000000000000000000 ) ) ;
#322=ORIENTED_EDGE ( 'NONE', *, *, #1688, .F. ) ;
#325=CIRCLE ( 'NONE', #4154, 1.800000000000000266 ) ;
#341=VECTOR ( 'NONE', #13220, 1000.000000000000114 ) ;
#465=DIRECTION ( 'NONE',  ( -0.000000000000000000, -1.000000000000000000, -0.000000000000000000 ) ) ;
#480=CARTESIAN_POINT ( 'NONE',  ( -3.000000000000000000, 41.00000000000000711, 9.013878188659973034 ) ) ;
#497=CARTESIAN_POINT ( 'NONE',  ( 1.845421771225094210, 38.60300962669240477, 9.323305159997634206 ) ) ;
#539=CARTESIAN_POINT ( 'NONE',  ( 0.7824566857511728868, 62.90282673968097527, 9.469691317190790159 ) ) ;
#548=VECTOR ( 'NONE', #4872, 1000.000000000000000 ) ;
#556=ADVANCED_BREP_SHAPE_REPRESENTATION ( '', ( #3094, #1488 ), #5315 ) ;
#560=CARTESIAN_POINT ( 'NONE',  ( -2.901926423773061536, 40.21397019809104023, 9.046021540735431188 ) ) ;
#604=CARTESIAN_POINT ( 'NONE',  ( 2.999999999999996003, 66.00000000000000000, 9.013878188659974811 ) ) ;
#620=CARTESIAN_POINT ( 'NONE',  ( 2.901926423773059760, 60.78602980190899530, 9.046021540735432964 ) ) ;
#635=ORIENTED_EDGE ( 'NONE', *, *, #7612, .T. ) ;
#637=AXIS2_PLACEMENT_3D ( 'NONE', #5603, #12227, #10673 ) ;
#703=EDGE_LOOP ( 'NONE', ( #14669, #2505 ) ) ;
#711=CARTESIAN_POINT ( 'NONE',  ( 0.9699764831012678279, 62.84572122215210754, 9.452135968713493597 ) ) ;
#812=CARTESIAN_POINT ( 'NONE',  ( 1.163414460601643398E-15, 38.00000000000000711, 9.500000000000000000 ) ) ;
#833=DIRECTION ( 'NONE',  ( 0.000000000000000000, -0.000000000000000000, 1.000000000000000000 ) ) ;
#840=CARTESIAN_POINT ( 'NONE',  ( -0.9714722756524757363, 62.84506667638981270, 9.451944983354374941 ) ) ;
#892=CARTESIAN_POINT ( 'NONE',  ( 1.163414459189985485E-15, 66.00000000000000000, 9.500000000000000000 ) ) ;
#893=AXIS2_PLACEMENT_3D ( 'NONE', #2743, #8238, #7973 ) ;
#919=AXIS2_PLACEMENT_3D ( 'NONE', #1143, #10501, #11876 ) ;
#953=CIRCLE ( 'NONE', #11923, 9.500000000000000000 ) ;
#975=ADVANCED_FACE ( 'NONE', ( #9394 ), #10508, .F. ) ;
#985=VERTEX_POINT ( 'NONE', #16002 ) ;
#1046=CARTESIAN_POINT ( 'NONE',  ( 1.163414459189985485E-15, 10.00000000000000000, 9.500000000000000000 ) ) ;
#1049=DIRECTION ( 'NONE',  ( -1.597771622610217359E-16, 1.000000000000000000, 0.000000000000000000 ) ) ;
#1086=EDGE_CURVE ( 'NONE', #4609, #9484, #7058, .T. ) ;
#1143=CARTESIAN_POINT ( 'NONE',  ( 0.000000000000000000, 0.000000000000000000, 0.000000000000000000 ) ) ;
#1175=EDGE_LOOP ( 'NONE', ( #12902, #13410, #14916, #4640, #5689, #1663, #8940, #6414 ) ) ;
#1202=AXIS2_PLACEMENT_3D ( 'NONE', #15389, #8864, #1049 ) ;
#1216=DIRECTION ( 'NONE',  ( -0.000000000000000000, -1.000000000000000000, -0.000000000000000000 ) ) ;
#1226=EDGE_LOOP ( 'NONE', ( #8728, #12309 ) ) ;
#1261=EDGE_CURVE ( 'NONE', #8474, #4810, #9019, .T. ) ;
#1274=ORIENTED_EDGE ( 'NONE', *, *, #12030, .T. ) ;
#1314=ADVANCED_FACE ( 'NONE', ( #14592 ), #16137, .T. ) ;
#1356=CARTESIAN_POINT ( 'NONE',  ( 0.000000000000000000, 65.20000000000000284, -5.741599279633704455E-16 ) ) ;
#1415=DIRECTION ( 'NONE',  ( 0.000000000000000000, 0.000000000000000000, 1.000000000000000000 ) ) ;
#1488=AXIS2_PLACEMENT_3D ( 'NONE', #3280, #8693, #15217 ) ;
#1498=CARTESIAN_POINT ( 'NONE',  ( 0.000000000000000000, 0.000000000000000000, 0.000000000000000000 ) ) ;
#1633=ADVANCED_FACE ( 'NONE', ( #16017 ), #3151, .F. ) ;
#1663=ORIENTED_EDGE ( 'NONE', *, *, #6779, .T. ) ;
#1688=EDGE_CURVE ( 'NONE', #985, #9484, #6238, .T. ) ;
#1726=EDGE_CURVE ( 'NONE', #7051, #8672, #11201, .T. ) ;
#1834=FACE_OUTER_BOUND ( 'NONE', #5360, .T. ) ;
#1841=ORIENTED_EDGE ( 'NONE', *, *, #16639, .F. ) ;
#1867=CARTESIAN_POINT ( 'NONE',  ( -1.734723475976807094E-15, 60.00000000000000711, 6.000000000000000000 ) ) ;
#1881=CARTESIAN_POINT ( 'NONE',  ( 0.000000000000000000, 66.00000000000000000, 0.9999999999999958922 ) ) ;
#1903=CARTESIAN_POINT ( 'NONE',  ( 0.000000000000000000, 66.00000000000000000, -9.500000000000000000 ) ) ;
#1919=CARTESIAN_POINT ( 'NONE',  ( -0.9699764831012689381, 38.15427877784792088, 9.452135968713491820 ) ) ;
#1949=CARTESIAN_POINT ( 'NONE',  ( -2.844883903241206546, 60.97223153686513086, 9.064373830433188672 ) ) ;
#1997=EDGE_LOOP ( 'NONE', ( #12559, #322, #14053, #5318 ) ) ;
#2022=AXIS2_PLACEMENT_3D ( 'NONE', #6899, #13453, #1415 ) ;
#2035=FACE_OUTER_BOUND ( 'NONE', #15996, .T. ) ;
#2106=ORIENTED_EDGE ( 'NONE', *, *, #5569, .F. ) ;
#2116=CARTESIAN_POINT ( 'NONE',  ( -2.903217335657449993, 60.78097370076725525, 9.045605051663343943 ) ) ;
#2144=EDGE_CURVE ( 'NONE', #8672, #11801, #12615, .T. ) ;
#2175=DIRECTION ( 'NONE',  ( 1.141265444721583757E-16, -1.000000000000000000, 0.000000000000000000 ) ) ;
#2202=DIRECTION ( 'NONE',  ( 0.000000000000000000, 0.000000000000000000, -1.000000000000000000 ) ) ;
#2217=DIRECTION ( 'NONE',  ( -0.000000000000000000, -0.000000000000000000, 1.000000000000000000 ) ) ;
#2251=CARTESIAN_POINT ( 'NONE',  ( 0.000000000000000000, 66.00000000000000000, -5.741599279633704455E-16 ) ) ;
#2282=CARTESIAN_POINT ( 'NONE',  ( 0.000000000000000000, 10.00000000000000000, -12.00000000000000178 ) ) ;
#2407=LINE ( 'NONE', #14266, #14703 ) ;
#2453=EDGE_LOOP ( 'NONE', ( #1841, #7875, #9989, #13838, #8877 ) ) ;
#2483=EDGE_LOOP ( 'NONE', ( #9993, #4850 ) ) ;
#2499=EDGE_LOOP ( 'NONE', ( #2690, #11700, #7081 ) ) ;
#2505=ORIENTED_EDGE ( 'NONE', *, *, #5403, .T. ) ;
#2535=DIRECTION ( 'NONE',  ( 0.000000000000000000, 0.7071067811865445751, 0.7071067811865504593 ) ) ;
#2635=FACE_BOUND ( 'NONE', #3168, .T. ) ;
#2655=( NAMED_UNIT ( * ) PLANE_ANGLE_UNIT ( ) SI_UNIT ( $, .RADIAN. ) );
#2674=ORIENTED_EDGE ( 'NONE', *, *, #4848, .F. ) ;
#2690=ORIENTED_EDGE ( 'NONE', *, *, #12030, .F. ) ;
#2716=ORIENTED_EDGE ( 'NONE', *, *, #5569, .T. ) ;
#2743=CARTESIAN_POINT ( 'NONE',  ( 0.000000000000000000, 66.00000000000000000, -5.741599279633704455E-16 ) ) ;
#2760=ORIENTED_EDGE ( 'NONE', *, *, #11941, .F. ) ;
#2777=FACE_OUTER_BOUND ( 'NONE', #15770, .T. ) ;
#2793=ADVANCED_FACE ( 'NONE', ( #4575 ), #9711, .F. ) ;
#2824=CARTESIAN_POINT ( 'NONE',  ( 1.224646799147347044E-16, 38.00000000000000711, -0.9999999999999956701 ) ) ;
#2925=UNCERTAINTY_MEASURE_WITH_UNIT (LENGTH_MEASURE( 1.000000000000000082E-05 ), #7545, 'distance_accuracy_value', 'NONE');
#2943=ORIENTED_EDGE ( 'NONE', *, *, #1261, .F. ) ;
#2995=ADVANCED_FACE ( 'NONE', ( #10324 ), #15561, .F. ) ;
#3051=FACE_OUTER_BOUND ( 'NONE', #16554, .T. ) ;
#3061=DIRECTION ( 'NONE',  ( -1.000000000000000000, -1.141265444721583757E-16, 0.000000000000000000 ) ) ;
#3077=ORIENTED_EDGE ( 'NONE', *, *, #5090, .F. ) ;
#3094=MANIFOLD_SOLID_BREP ( 'Cut-Extrude1', #12930 ) ;
#3100=CIRCLE ( 'NONE', #14894, 3.000000000000000000 ) ;
#3124=CIRCLE ( 'NONE', #919, 12.00000000000000178 ) ;
#3140=AXIS2_PLACEMENT_3D ( 'NONE', #6341, #11596, #5146 ) ;
#3151=CYLINDRICAL_SURFACE ( 'NONE', #11198, 2.999999999999999556 ) ;
#3168=EDGE_LOOP ( 'NONE', ( #16077, #3905 ) ) ;
#3251=CARTESIAN_POINT ( 'NONE',  ( -2.601523022692215026, 61.50677485111217635, 9.137549538570182150 ) ) ;
#3277=PRODUCT_CONTEXT ( 'NONE', #6196, 'mechanical' ) ;
#3280=CARTESIAN_POINT ( 'NONE',  ( 0.000000000000000000, 0.000000000000000000, 0.000000000000000000 ) ) ;
#3300=CARTESIAN_POINT ( 'NONE',  ( -2.844582250340501162, 40.02709031926097083, 9.064464814046603536 ) ) ;
#3305=DIRECTION ( 'NONE',  ( -0.000000000000000000, 1.000000000000000000, -0.000000000000000000 ) ) ;
#3385=CARTESIAN_POINT ( 'NONE',  ( -1.334572366541263433, 38.30595095619238322, 9.407584458684455697 ) ) ;
#3389=CARTESIAN_POINT ( 'NONE',  ( -3.000000000000002220, 60.00000000000000711, 6.000000000000000000 ) ) ;
#3500=CARTESIAN_POINT ( 'NONE',  ( -0.7808854937525574469, 62.90333651941379145, 9.469847369592788056 ) ) ;
#3508=LINE ( 'NONE', #5826, #548 ) ;
#3538=CARTESIAN_POINT ( 'NONE',  ( 0.000000000000000000, 38.00000000000000711, -5.741599279633704455E-16 ) ) ;
#3558=CARTESIAN_POINT ( 'NONE',  ( 0.000000000000000000, 65.20000000000000284, -5.741599279633704455E-16 ) ) ;
#3562=CARTESIAN_POINT ( 'NONE',  ( 0.1969510947806087375, 63.00000000000001421, 9.500000000000003553 ) ) ;
#3572=EDGE_LOOP ( 'NONE', ( #7752, #5678 ) ) ;
#3578=ORIENTED_EDGE ( 'NONE', *, *, #14271, .F. ) ;
#3599=ORIENTED_EDGE ( 'NONE', *, *, #6284, .F. ) ;
#3604=AXIS2_PLACEMENT_3D ( 'NONE', #8282, #5709, #16015 ) ;
#3618=AXIS2_PLACEMENT_3D ( 'NONE', #4378, #4298, #14689 ) ;
#3628=ORIENTED_EDGE ( 'NONE', *, *, #14796, .F. ) ;
#3643=DIRECTION ( 'NONE',  ( 0.000000000000000000, 0.000000000000000000, 1.000000000000000000 ) ) ;
#3706=EDGE_CURVE ( 'NONE', #11572, #11419, #9252, .T. ) ;
#3718=ORIENTED_EDGE ( 'NONE', *, *, #2144, .T. ) ;
#3739=CARTESIAN_POINT ( 'NONE',  ( 2.999999999999996891, 60.00000000000000711, 9.013878188659974811 ) ) ;
#3777=CARTESIAN_POINT ( 'NONE',  ( -3.000000000000003109, 60.00000000000000711, 9.013878188659973034 ) ) ;
#3785=ADVANCED_FACE ( 'NONE', ( #9590 ), #5637, .F. ) ;
#3905=ORIENTED_EDGE ( 'NONE', *, *, #13504, .F. ) ;
#3912=ORIENTED_EDGE ( 'NONE', *, *, #12768, .T. ) ;
#3916=CARTESIAN_POINT ( 'NONE',  ( 0.000000000000000000, 10.00000000000000000, -9.500000000000000000 ) ) ;
#3955=STYLED_ITEM ( 'NONE', ( #9638 ), #3094 ) ;
#4018=PRODUCT_DEFINITION ( 'UNKNOWN', '', #4254, #9300 ) ;
#4057=ORIENTED_EDGE ( 'NONE', *, *, #11829, .T. ) ;
#4077=DIRECTION ( 'NONE',  ( -0.000000000000000000, 1.000000000000000000, -0.000000000000000000 ) ) ;
#4154=AXIS2_PLACEMENT_3D ( 'NONE', #2251, #4913, #16356 ) ;
#4254=PRODUCT_DEFINITION_FORMATION_WITH_SPECIFIED_SOURCE ( 'ANY', '', #16847, .NOT_KNOWN. ) ;
#4288=VECTOR ( 'NONE', #9575, 1000.000000000000000 ) ;
#4298=DIRECTION ( 'NONE',  ( -0.000000000000000000, -1.000000000000000000, -0.000000000000000000 ) ) ;
#4302=CIRCLE ( 'NONE', #13630, 0.9999999999999983347 ) ;
#4306=FACE_OUTER_BOUND ( 'NONE', #6269, .T. ) ;
#4343=LINE ( 'NONE', #6890, #4288 ) ;
#4378=CARTESIAN_POINT ( 'NONE',  ( 0.000000000000000000, 66.00000000000000000, 0.000000000000000000 ) ) ;
#4424=CARTESIAN_POINT ( 'NONE',  ( -2.694300560877699535, 39.66622868771214883, 9.110264267939502503 ) ) ;
#4451=CARTESIAN_POINT ( 'NONE',  ( 0.000000000000000000, 66.00000000000000000, -5.741599279633704455E-16 ) ) ;
#4478=VECTOR ( 'NONE', #465, 1000.000000000000000 ) ;
#4481=SHAPE_DEFINITION_REPRESENTATION ( #11358, #6937 ) ;
#4575=FACE_OUTER_BOUND ( 'NONE', #15345, .T. ) ;
#4604=CARTESIAN_POINT ( 'NONE',  ( 2.844883903241205214, 40.02776846313489045, 9.064373830433188672 ) ) ;
#4609=VERTEX_POINT ( 'NONE', #2824 ) ;
#4634=CARTESIAN_POINT ( 'NONE',  ( 2.999999999999996891, 60.00000000000000711, 9.013878188659974811 ) ) ;
#4640=ORIENTED_EDGE ( 'NONE', *, *, #11099, .T. ) ;
#4676=DIRECTION ( 'NONE',  ( 1.000000000000000000, 0.000000000000000000, -0.000000000000000000 ) ) ;
#4721=CARTESIAN_POINT ( 'NONE',  ( 2.259918635623968441, 61.98265998586796854, 9.228371864727256124 ) ) ;
#4727=DIRECTION ( 'NONE',  ( 1.049727191138612163E-16, 0.5150380749100629263, -0.8571673007021070045 ) ) ;
#4810=VERTEX_POINT ( 'NONE', #11560 ) ;
#4848=EDGE_CURVE ( 'NONE', #15887, #15487, #10298, .T. ) ;
#4850=ORIENTED_EDGE ( 'NONE', *, *, #15396, .F. ) ;
#4856=FACE_OUTER_BOUND ( 'NONE', #703, .T. ) ;
#4872=DIRECTION ( 'NONE',  ( 0.000000000000000000, 1.000000000000000000, 0.000000000000000000 ) ) ;
#4913=DIRECTION ( 'NONE',  ( -0.000000000000000000, 1.000000000000000000, -0.000000000000000000 ) ) ;
#4950=PLANE ( 'NONE',  #6329 ) ;
#5031=CARTESIAN_POINT ( 'NONE',  ( 2.204364238465236069E-16, 66.00000000000000000, -1.800000000000000711 ) ) ;
#5037=DIRECTION ( 'NONE',  ( 0.000000000000000000, 0.000000000000000000, 1.000000000000000000 ) ) ;
#5090=EDGE_CURVE ( 'NONE', #7931, #214, #14646, .T. ) ;
#5146=DIRECTION ( 'NONE',  ( 0.000000000000000000, 0.000000000000000000, 1.000000000000000000 ) ) ;
#5184=ADVANCED_FACE ( 'NONE', ( #8299 ), #11215, .T. ) ;
#5279=EDGE_LOOP ( 'NONE', ( #9386, #4057, #8181, #3599 ) ) ;
#5293=CARTESIAN_POINT ( 'NONE',  ( 2.999999999999996891, 60.00000000000000711, 6.000000000000000000 ) ) ;
#5315=( GEOMETRIC_REPRESENTATION_CONTEXT ( 3 ) GLOBAL_UNCERTAINTY_ASSIGNED_CONTEXT ( ( #2925 ) ) GLOBAL_UNIT_ASSIGNED_CONTEXT ( ( #7545, #2655, #7887 ) ) REPRESENTATION_CONTEXT ( 'NONE', 'WORKASPACE' ) );
#5316=CIRCLE ( 'NONE', #7503, 0.9999999999999950040 ) ;
#5318=ORIENTED_EDGE ( 'NONE', *, *, #10215, .T. ) ;
#5343=DIRECTION ( 'NONE',  ( -0.000000000000000000, 1.000000000000000000, -0.000000000000000000 ) ) ;
#5352=DIRECTION ( 'NONE',  ( 0.000000000000000000, 1.000000000000000000, 0.000000000000000000 ) ) ;
#5355=CYLINDRICAL_SURFACE ( 'NONE', #13736, 0.9999999999999965583 ) ;
#5360=EDGE_LOOP ( 'NONE', ( #6869, #635, #12486, #16034 ) ) ;
#5372=CARTESIAN_POINT ( 'NONE',  ( 2.999999999999996891, 60.00000000000000711, 6.000000000000000000 ) ) ;
#5390=DIRECTION ( 'NONE',  ( 0.000000000000000000, 0.000000000000000000, 1.000000000000000000 ) ) ;
#5403=EDGE_CURVE ( 'NONE', #12347, #16344, #14704, .T. ) ;
#5457=VERTEX_POINT ( 'NONE', #14555 ) ;
#5569=EDGE_CURVE ( 'NONE', #11572, #7931, #4343, .T. ) ;
#5577=CIRCLE ( 'NONE', #13826, 2.999999999999999556 ) ;
#5603=CARTESIAN_POINT ( 'NONE',  ( 0.000000000000000000, 66.00000000000000000, -5.741599279633704455E-16 ) ) ;
#5637=PLANE ( 'NONE',  #14376 ) ;
#5641=CARTESIAN_POINT ( 'NONE',  ( 2.693790225569809849, 39.66504951222130870, 9.110418847747206783 ) ) ;
#5678=ORIENTED_EDGE ( 'NONE', *, *, #16907, .T. ) ;
#5689=ORIENTED_EDGE ( 'NONE', *, *, #5090, .T. ) ;
#5709=DIRECTION ( 'NONE',  ( -0.000000000000000000, -1.000000000000000000, -0.000000000000000000 ) ) ;
#5765=DIRECTION ( 'NONE',  ( -0.000000000000000000, 1.000000000000000000, -0.000000000000000000 ) ) ;
#5820=CARTESIAN_POINT ( 'NONE',  ( 0.000000000000000000, 66.00000000000000000, 1.799999999999999600 ) ) ;
#5826=CARTESIAN_POINT ( 'NONE',  ( -3.000000000000003109, 66.00000000000000000, 9.013878188659973034 ) ) ;
#5827=VECTOR ( 'NONE', #11076, 1000.000000000000000 ) ;
#5832=ORIENTED_EDGE ( 'NONE', *, *, #14271, .T. ) ;
#5891=CARTESIAN_POINT ( 'NONE',  ( 2.383743612111322463, 39.16804506571254763, 9.196765735797566066 ) ) ;
#5955=CARTESIAN_POINT ( 'NONE',  ( -1.831162533324883990, 38.61573685184089300, 9.323294315095141727 ) ) ;
#5987=DIRECTION ( 'NONE',  ( -0.000000000000000000, 1.000000000000000000, -0.000000000000000000 ) ) ;
#6014=EDGE_CURVE ( 'NONE', #9484, #985, #4302, .T. ) ;
#6028=CARTESIAN_POINT ( 'NONE',  ( -1.507804506096813046, 38.39915541515519237, 9.381017998102995747 ) ) ;
#6057=LINE ( 'NONE', #11304, #16094 ) ;
#6196=APPLICATION_CONTEXT ( 'automotive_design' ) ;
#6238=CIRCLE ( 'NONE', #9565, 0.9999999999999983347 ) ;
#6258=CARTESIAN_POINT ( 'NONE',  ( 1.224646799147351235E-16, 65.20000000000000284, -0.9999999999999988898 ) ) ;
#6269=EDGE_LOOP ( 'NONE', ( #16532, #15877, #14043, #8454 ) ) ;
#6284=EDGE_CURVE ( 'NONE', #16344, #11779, #6057, .T. ) ;
#6329=AXIS2_PLACEMENT_3D ( 'NONE', #10295, #16715, #10202 ) ;
#6341=CARTESIAN_POINT ( 'NONE',  ( 0.000000000000000000, 0.000000000000000000, 0.000000000000000000 ) ) ;
#6414=ORIENTED_EDGE ( 'NONE', *, *, #11799, .F. ) ;
#6580=FACE_OUTER_BOUND ( 'NONE', #1997, .T. ) ;
#6583=CARTESIAN_POINT ( 'NONE',  ( 0.000000000000000000, 38.00000000000000711, 0.9999999999999943379 ) ) ;
#6601=VERTEX_POINT ( 'NONE', #1046 ) ;
#6630=ORIENTED_EDGE ( 'NONE', *, *, #6284, .T. ) ;
#6689=ORIENTED_EDGE ( 'NONE', *, *, #13807, .F. ) ;
#6716=CARTESIAN_POINT ( 'NONE',  ( 0.000000000000000000, 66.00000000000000000, -9.500000000000000000 ) ) ;
#6731=CYLINDRICAL_SURFACE ( 'NONE', #3604, 12.00000000000000178 ) ;
#6736=DIRECTION ( 'NONE',  ( -0.000000000000000000, -0.000000000000000000, 1.000000000000000000 ) ) ;
#6779=EDGE_CURVE ( 'NONE', #214, #6601, #2407, .T. ) ;
#6813=CARTESIAN_POINT ( 'NONE',  ( -1.734723475976807094E-15, 60.00000000000000711, 6.000000000000000000 ) ) ;
#6869=ORIENTED_EDGE ( 'NONE', *, *, #6014, .F. ) ;
#6890=CARTESIAN_POINT ( 'NONE',  ( 3.000000000000000000, 41.00000000000000711, 6.000000000000000000 ) ) ;
#6899=CARTESIAN_POINT ( 'NONE',  ( 0.000000000000000000, 10.00000000000000000, 0.000000000000000000 ) ) ;
#6931=AXIS2_PLACEMENT_3D ( 'NONE', #1498, #5352, #13267 ) ;
#6937=SHAPE_REPRESENTATION ( 'Servo-Axe', ( #1488 ), #5315 ) ;
#6989=CARTESIAN_POINT ( 'NONE',  ( -2.600106608147766174, 39.49089379158813529, 9.137947797636652325 ) ) ;
#7017=CARTESIAN_POINT ( 'NONE',  ( -2.980268877975830399, 60.39571231257155404, 9.020512128682495856 ) ) ;
#7047=EDGE_LOOP ( 'NONE', ( #2106, #3628, #3718, #3578, #3077 ) ) ;
#7051=VERTEX_POINT ( 'NONE', #11084 ) ;
#7058=LINE ( 'NONE', #13689, #14344 ) ;
#7081=ORIENTED_EDGE ( 'NONE', *, *, #15827, .T. ) ;
#7146=CARTESIAN_POINT ( 'NONE',  ( -1.734723475976807094E-15, 60.00000000000000711, 6.000000000000000000 ) ) ;
#7172=CARTESIAN_POINT ( 'NONE',  ( -0.1972064085032595726, 63.00000000000000000, 9.500000000000001776 ) ) ;
#7175=AXIS2_PLACEMENT_3D ( 'NONE', #13847, #14009, #7303 ) ;
#7178=VERTEX_POINT ( 'NONE', #3777 ) ;
#7286=EDGE_CURVE ( 'NONE', #11419, #8068, #10635, .T. ) ;
#7292=SURFACE_STYLE_FILL_AREA ( #8431 ) ;
#7300=AXIS2_PLACEMENT_3D ( 'NONE', #8573, #10032, #2202 ) ;
#7303=DIRECTION ( 'NONE',  ( 1.000000000000000000, 0.000000000000000000, 0.000000000000000000 ) ) ;
#7337=CARTESIAN_POINT ( 'NONE',  ( 1.163414460601643398E-15, 38.00000000000000711, 9.500000000000000000 ) ) ;
#7378=CARTESIAN_POINT ( 'NONE',  ( 2.383085342081995517, 61.83271933867543169, 9.196931476227284463 ) ) ;
#7388=DIRECTION ( 'NONE',  ( -0.000000000000000000, 1.000000000000000000, -0.000000000000000000 ) ) ;
#7416=ADVANCED_FACE ( 'NONE', ( #2035 ), #16304, .T. ) ;
#7453=ORIENTED_EDGE ( 'NONE', *, *, #9315, .T. ) ;
#7503=AXIS2_PLACEMENT_3D ( 'NONE', #13348, #5343, #15991 ) ;
#7525=CARTESIAN_POINT ( 'NONE',  ( 0.000000000000000000, 66.00000000000000000, 0.000000000000000000 ) ) ;
#7545=( LENGTH_UNIT ( ) NAMED_UNIT ( * ) SI_UNIT ( .MILLI., .METRE. ) );
#7612=EDGE_CURVE ( 'NONE', #9484, #8747, #16027, .T. ) ;
#7731=ORIENTED_EDGE ( 'NONE', *, *, #1086, .T. ) ;
#7752=ORIENTED_EDGE ( 'NONE', *, *, #4848, .T. ) ;
#7773=ORIENTED_EDGE ( 'NONE', *, *, #12048, .F. ) ;
#7875=ORIENTED_EDGE ( 'NONE', *, *, #15354, .F. ) ;
#7887=( NAMED_UNIT ( * ) SI_UNIT ( $, .STERADIAN. ) SOLID_ANGLE_UNIT ( ) );
#7919=ORIENTED_EDGE ( 'NONE', *, *, #11829, .F. ) ;
#7931=VERTEX_POINT ( 'NONE', #16860 ) ;
#7973=DIRECTION ( 'NONE',  ( 0.000000000000000000, 0.000000000000000000, 1.000000000000000000 ) ) ;
#8011=DIRECTION ( 'NONE',  ( 0.000000000000000000, 0.000000000000000000, 1.000000000000000000 ) ) ;
#8065=COLOUR_RGB ( '', 0.72549020, 0.75294118, 0.79215686) ;
#8068=VERTEX_POINT ( 'NONE', #3739 ) ;
#8181=ORIENTED_EDGE ( 'NONE', *, *, #12153, .T. ) ;
#8182=CARTESIAN_POINT ( 'NONE',  ( -3.000000000000000000, 41.00000000000000711, 9.013878188659973034 ) ) ;
#8183=VECTOR ( 'NONE', #2175, 1000.000000000000000 ) ;
#8231=B_SPLINE_CURVE_WITH_KNOTS ( 'NONE', 3,
 ( #15326, #3562, #8799, #539, #711, #8438, #13928, #8694, #11253, #4721, #7378, #13600, #9814, #13678, #620, #16488, #9981, #4634 ),
 .UNSPECIFIED., .F., .F.,
 ( 4, 2, 2, 2, 2, 2, 2, 2, 4 ),
 ( 0.004721323624227211080, 0.005310725018217473184, 0.005900126412207735288, 0.006489527806197996525, 0.007078929200188269905, 0.007668330594178543284, 0.008257731988168816664, 0.008847133382159089177, 0.009436534776149363424 ),
 .UNSPECIFIED. ) ;
#8238=DIRECTION ( 'NONE',  ( -0.000000000000000000, 1.000000000000000000, -0.000000000000000000 ) ) ;
#8282=CARTESIAN_POINT ( 'NONE',  ( 0.000000000000000000, 10.00000000000000000, 0.000000000000000000 ) ) ;
#8283=DIRECTION ( 'NONE',  ( 0.000000000000000000, 0.000000000000000000, 1.000000000000000000 ) ) ;
#8299=FACE_OUTER_BOUND ( 'NONE', #11875, .T. ) ;
#8339=SURFACE_STYLE_USAGE ( .BOTH. , #13836 ) ;
#8354=ORIENTED_EDGE ( 'NONE', *, *, #11799, .T. ) ;
#8362=AXIS2_PLACEMENT_3D ( 'NONE', #3538, #14010, #8776 ) ;
#8398=CARTESIAN_POINT ( 'NONE',  ( 0.7808854937525596673, 38.09666348058623697, 9.469847369592788056 ) ) ;
#8421=ORIENTED_EDGE ( 'NONE', *, *, #13720, .T. ) ;
#8431=FILL_AREA_STYLE ('',( #8687 ) ) ;
#8432=ORIENTED_EDGE ( 'NONE', *, *, #9315, .F. ) ;
#8438=CARTESIAN_POINT ( 'NONE',  ( 1.334572366541260990, 62.69404904380762389, 9.407584458684453921 ) ) ;
#8454=ORIENTED_EDGE ( 'NONE', *, *, #1688, .T. ) ;
#8455=CARTESIAN_POINT ( 'NONE',  ( -0.1969510947806061563, 38.00000000000000711, 9.500000000000003553 ) ) ;
#8474=VERTEX_POINT ( 'NONE', #12100 ) ;
#8573=CARTESIAN_POINT ( 'NONE',  ( 0.000000000000000000, 66.00000000000000000, 0.000000000000000000 ) ) ;
#8603=CIRCLE ( 'NONE', #9978, 9.500000000000000000 ) ;
#8625=VERTEX_POINT ( 'NONE', #5820 ) ;
#8630=AXIS2_PLACEMENT_3D ( 'NONE', #9817, #15122, #12304 ) ;
#8647=CARTESIAN_POINT ( 'NONE',  ( 0.9714722756524812874, 38.15493332361022283, 9.451944983354378493 ) ) ;
#8650=CARTESIAN_POINT ( 'NONE',  ( 0.000000000000000000, 10.00000000000000000, 0.000000000000000000 ) ) ;
#8652=ORIENTED_EDGE ( 'NONE', *, *, #11611, .T. ) ;
#8658=CARTESIAN_POINT ( 'NONE',  ( -1.512611822017144947, 62.62004896476273785, 9.385845453595075938 ) ) ;
#8659=AXIS2_PLACEMENT_3D ( 'NONE', #7525, #13037, #15274 ) ;
#8661=CARTESIAN_POINT ( 'NONE',  ( 1.163414460601643398E-15, 38.00000000000000711, 9.500000000000000000 ) ) ;
#8672=VERTEX_POINT ( 'NONE', #9951 ) ;
#8687=FILL_AREA_STYLE_COLOUR ( '', #8065 ) ;
#8693=DIRECTION ( 'NONE',  ( 0.000000000000000000, 0.000000000000000000, 1.000000000000000000 ) ) ;
#8694=CARTESIAN_POINT ( 'NONE',  ( 1.831162533324887542, 62.38426314815912832, 9.323294315095143503 ) ) ;
#8728=ORIENTED_EDGE ( 'NONE', *, *, #11611, .F. ) ;
#8735=FACE_BOUND ( 'NONE', #2483, .T. ) ;
#8742=VECTOR ( 'NONE', #2217, 1000.000000000000000 ) ;
#8747=VERTEX_POINT ( 'NONE', #5031 ) ;
#8769=AXIS2_PLACEMENT_3D ( 'NONE', #10065, #5765, #12470 ) ;
#8776=DIRECTION ( 'NONE',  ( 0.000000000000000000, 0.000000000000000000, 1.000000000000000000 ) ) ;
#8799=CARTESIAN_POINT ( 'NONE',  ( 0.3969782420128937228, 62.98010902838336023, 9.493666329891928157 ) ) ;
#8837=DIRECTION ( 'NONE',  ( 0.000000000000000000, 0.000000000000000000, 1.000000000000000000 ) ) ;
#8864=DIRECTION ( 'NONE',  ( 1.000000000000000000, 1.597771622610217359E-16, 0.000000000000000000 ) ) ;
#8877=ORIENTED_EDGE ( 'NONE', *, *, #12768, .F. ) ;
#8940=ORIENTED_EDGE ( 'NONE', *, *, #15396, .T. ) ;
#9019=LINE ( 'NONE', #6583, #341 ) ;
#9067=AXIS2_PLACEMENT_3D ( 'NONE', #11980, #218, #10682 ) ;
#9081=AXIS2_PLACEMENT_3D ( 'NONE', #8650, #15172, #833 ) ;
#9109=DIRECTION ( 'NONE',  ( 0.000000000000000000, 1.000000000000000000, 0.000000000000000000 ) ) ;
#9159=CIRCLE ( 'NONE', #3140, 12.00000000000000178 ) ;
#9183=ORIENTED_EDGE ( 'NONE', *, *, #16639, .T. ) ;
#9252=LINE ( 'NONE', #5372, #15204 ) ;
#9300=PRODUCT_DEFINITION_CONTEXT ( 'detailed design', #13243, 'design' ) ;
#9314=ADVANCED_FACE ( 'NONE', ( #2777 ), #5355, .F. ) ;
#9315=EDGE_CURVE ( 'NONE', #4609, #4810, #12, .T. ) ;
#9386=ORIENTED_EDGE ( 'NONE', *, *, #5403, .F. ) ;
#9394=FACE_OUTER_BOUND ( 'NONE', #1226, .T. ) ;
#9410=CARTESIAN_POINT ( 'NONE',  ( -3.000000000000002220, 60.00000000000000711, 6.000000000000000000 ) ) ;
#9431=VERTEX_POINT ( 'NONE', #15630 ) ;
#9448=MECHANICAL_DESIGN_GEOMETRIC_PRESENTATION_REPRESENTATION('',(#3955),#15735);
#9484=VERTEX_POINT ( 'NONE', #6258 ) ;
#9565=AXIS2_PLACEMENT_3D ( 'NONE', #3558, #3305, #3643 ) ;
#9575=DIRECTION ( 'NONE',  ( -0.000000000000000000, -0.000000000000000000, 1.000000000000000000 ) ) ;
#9590=FACE_OUTER_BOUND ( 'NONE', #11835, .T. ) ;
#9626=UNCERTAINTY_MEASURE_WITH_UNIT (LENGTH_MEASURE( 1.000000000000000082E-05 ), #9724, 'distance_accuracy_value', 'NONE');
#9638=PRESENTATION_STYLE_ASSIGNMENT (( #8339 ) ) ;
#9669=CARTESIAN_POINT ( 'NONE',  ( -0.7824566857511718876, 38.09717326031902473, 9.469691317190788382 ) ) ;
#9696=DIRECTION ( 'NONE',  ( -0.000000000000000000, -1.000000000000000000, -0.000000000000000000 ) ) ;
#9711=CONICAL_SURFACE ( 'NONE', #15461, 0.9999999999999950040, 1.029744258676644320 ) ;
#9724=( LENGTH_UNIT ( ) NAMED_UNIT ( * ) SI_UNIT ( .MILLI., .METRE. ) );
#9744=DIRECTION ( 'NONE',  ( -0.000000000000000000, -1.000000000000000000, -0.000000000000000000 ) ) ;
#9760=ADVANCED_FACE ( 'NONE', ( #8735, #4856 ), #13883, .T. ) ;
#9782=AXIS2_PLACEMENT_3D ( 'NONE', #14474, #10685, #14642 ) ;
#9785=LINE ( 'NONE', #14304, #10699 ) ;
#9814=CARTESIAN_POINT ( 'NONE',  ( 2.694300560877697759, 61.33377131228787249, 9.110264267939502503 ) ) ;
#9817=CARTESIAN_POINT ( 'NONE',  ( 0.000000000000000000, 10.00000000000000000, 0.000000000000000000 ) ) ;
#9820=LINE ( 'NONE', #15046, #11345 ) ;
#9869=LINE ( 'NONE', #1881, #16168 ) ;
#9901=DIRECTION ( 'NONE',  ( 0.000000000000000000, 0.000000000000000000, 1.000000000000000000 ) ) ;
#9946=CARTESIAN_POINT ( 'NONE',  ( -1.845421771225094876, 62.39699037330763076, 9.323305159997635982 ) ) ;
#9951=CARTESIAN_POINT ( 'NONE',  ( -3.000000000000000000, 41.00000000000000711, 6.000000000000000000 ) ) ;
#9978=AXIS2_PLACEMENT_3D ( 'NONE', #13955, #12494, #11203 ) ;
#9981=CARTESIAN_POINT ( 'NONE',  ( 2.999999999999998668, 60.19942049011861940, 9.013878188659973034 ) ) ;
#9985=AXIS2_PLACEMENT_3D ( 'NONE', #8, #15632, #14350 ) ;
#9989=ORIENTED_EDGE ( 'NONE', *, *, #7286, .T. ) ;
#9993=ORIENTED_EDGE ( 'NONE', *, *, #16214, .F. ) ;
#10032=DIRECTION ( 'NONE',  ( -0.000000000000000000, -1.000000000000000000, -0.000000000000000000 ) ) ;
#10065=CARTESIAN_POINT ( 'NONE',  ( 0.000000000000000000, 66.00000000000000000, -5.741599279633704455E-16 ) ) ;
#10141=ADVANCED_FACE ( 'NONE', ( #3051 ), #6731, .T. ) ;
#10202=DIRECTION ( 'NONE',  ( 0.000000000000000000, -0.000000000000000000, 1.000000000000000000 ) ) ;
#10215=EDGE_CURVE ( 'NONE', #8625, #8747, #325, .T. ) ;
#10224=SHAPE_REPRESENTATION_RELATIONSHIP ( 'NONE' , 'NONE' ,  #6937, #556 ) ;
#10234=VECTOR ( 'NONE', #9744, 1000.000000000000000 ) ;
#10295=CARTESIAN_POINT ( 'NONE',  ( 0.000000000000000000, 66.00000000000000000, 0.000000000000000000 ) ) ;
#10298=CIRCLE ( 'NONE', #8659, 9.500000000000000000 ) ;
#10324=FACE_OUTER_BOUND ( 'NONE', #15380, .T. ) ;
#10456=DIRECTION ( 'NONE',  ( 1.000000000000000000, 0.000000000000000000, 0.000000000000000000 ) ) ;
#10501=DIRECTION ( 'NONE',  ( 0.000000000000000000, 1.000000000000000000, 0.000000000000000000 ) ) ;
#10508=PLANE ( 'NONE',  #6931 ) ;
#10537=CARTESIAN_POINT ( 'NONE',  ( 2.980268877975829511, 40.60428768742846728, 9.020512128682495856 ) ) ;
#10601=CARTESIAN_POINT ( 'NONE',  ( 0.000000000000000000, 66.00000000000000000, -5.741599279633704455E-16 ) ) ;
#10635=LINE ( 'NONE', #13396, #13642 ) ;
#10673=DIRECTION ( 'NONE',  ( 0.000000000000000000, 0.000000000000000000, 1.000000000000000000 ) ) ;
#10682=DIRECTION ( 'NONE',  ( 0.000000000000000000, 0.000000000000000000, 1.000000000000000000 ) ) ;
#10685=DIRECTION ( 'NONE',  ( 0.000000000000000000, 1.000000000000000000, 0.000000000000000000 ) ) ;
#10687=CIRCLE ( 'NONE', #8769, 1.800000000000000266 ) ;
#10699=VECTOR ( 'NONE', #2535, 1000.000000000000000 ) ;
#10702=ADVANCED_FACE ( 'NONE', ( #11256 ), #11098, .F. ) ;
#10705=CARTESIAN_POINT ( 'NONE',  ( 3.000000000000000000, 41.00000000000000711, 9.013878188659973034 ) ) ;
#10756=LINE ( 'NONE', #6716, #10234 ) ;
#10828=DIRECTION ( 'NONE',  ( 0.000000000000000000, 0.000000000000000000, 1.000000000000000000 ) ) ;
#10963=ADVANCED_FACE ( 'NONE', ( #4306 ), #14782, .F. ) ;
#10964=CARTESIAN_POINT ( 'NONE',  ( 2.601523022692213694, 39.49322514888784497, 9.137549538570182150 ) ) ;
#11076=DIRECTION ( 'NONE',  ( -0.000000000000000000, -1.000000000000000000, -0.000000000000000000 ) ) ;
#11084=CARTESIAN_POINT ( 'NONE',  ( -3.000000000000002220, 60.00000000000000711, 6.000000000000000000 ) ) ;
#11098=CYLINDRICAL_SURFACE ( 'NONE', #7175, 3.000000000000000000 ) ;
#11099=EDGE_CURVE ( 'NONE', #8068, #7931, #13662, .T. ) ;
#11118=AXIS2_PLACEMENT_3D ( 'NONE', #1867, #16450, #4676 ) ;
#11146=CARTESIAN_POINT ( 'NONE',  ( -3.000000000000003109, 60.00000000000000711, 9.013878188659973034 ) ) ;
#11181=ORIENTED_EDGE ( 'NONE', *, *, #3706, .F. ) ;
#11197=CARTESIAN_POINT ( 'NONE',  ( -2.383085342081997293, 39.16728066132458963, 9.196931476227280911 ) ) ;
#11198=AXIS2_PLACEMENT_3D ( 'NONE', #7146, #13626, #12072 ) ;
#11201=LINE ( 'NONE', #3389, #8183 ) ;
#11203=DIRECTION ( 'NONE',  ( 0.000000000000000000, 0.000000000000000000, 1.000000000000000000 ) ) ;
#11215=PLANE ( 'NONE',  #11118 ) ;
#11226=CARTESIAN_POINT ( 'NONE',  ( 1.163414457778310218E-15, 63.00000000000000000, 9.500000000000000000 ) ) ;
#11253=CARTESIAN_POINT ( 'NONE',  ( 1.983673311716144694, 62.25902922769662240, 9.291669371308648451 ) ) ;
#11256=FACE_OUTER_BOUND ( 'NONE', #7047, .T. ) ;
#11257=CYLINDRICAL_SURFACE ( 'NONE', #8630, 12.00000000000000178 ) ;
#11260=CARTESIAN_POINT ( 'NONE',  ( 1.224646799147347044E-16, 38.00000000000000711, -0.9999999999999956701 ) ) ;
#11272=CARTESIAN_POINT ( 'NONE',  ( -0.3969782420128915579, 38.01989097161666109, 9.493666329891928157 ) ) ;
#11293=ORIENTED_EDGE ( 'NONE', *, *, #6014, .T. ) ;
#11304=CARTESIAN_POINT ( 'NONE',  ( 0.000000000000000000, 10.00000000000000000, -12.00000000000000178 ) ) ;
#11327=CARTESIAN_POINT ( 'NONE',  ( -3.000000000000000000, 41.00000000000000711, 6.000000000000000000 ) ) ;
#11345=VECTOR ( 'NONE', #16668, 1000.000000000000000 ) ;
#11358=PRODUCT_DEFINITION_SHAPE ( 'NONE', 'NONE',  #4018 ) ;
#11419=VERTEX_POINT ( 'NONE', #5293 ) ;
#11424=ORIENTED_EDGE ( 'NONE', *, *, #14796, .T. ) ;
#11501=DIRECTION ( 'NONE',  ( -0.000000000000000000, 1.000000000000000000, -0.000000000000000000 ) ) ;
#11560=CARTESIAN_POINT ( 'NONE',  ( 0.000000000000000000, 38.00000000000000711, 0.9999999999999943379 ) ) ;
#11572=VERTEX_POINT ( 'NONE', #14033 ) ;
#11581=ORIENTED_EDGE ( 'NONE', *, *, #6779, .F. ) ;
#11596=DIRECTION ( 'NONE',  ( 0.000000000000000000, 1.000000000000000000, 0.000000000000000000 ) ) ;
#11611=EDGE_CURVE ( 'NONE', #11779, #9431, #3124, .T. ) ;
#11700=ORIENTED_EDGE ( 'NONE', *, *, #1261, .T. ) ;
#11736=ADVANCED_FACE ( 'NONE', ( #1834 ), #11874, .F. ) ;
#11737=DIRECTION ( 'NONE',  ( -1.597771622610217359E-16, 1.000000000000000000, -0.000000000000000000 ) ) ;
#11779=VERTEX_POINT ( 'NONE', #15903 ) ;
#11799=EDGE_CURVE ( 'NONE', #15887, #16595, #10756, .T. ) ;
#11801=VERTEX_POINT ( 'NONE', #8182 ) ;
#11829=EDGE_CURVE ( 'NONE', #12347, #9431, #14626, .T. ) ;
#11835=EDGE_LOOP ( 'NONE', ( #12563, #14873, #9183, #15078 ) ) ;
#11842=CONICAL_SURFACE ( 'NONE', #13224, 1.800000000000000266, 0.7853981633974524978 ) ;
#11874=CONICAL_SURFACE ( 'NONE', #637, 1.800000000000000266, 0.7853981633974524978 ) ;
#11875=EDGE_LOOP ( 'NONE', ( #12846, #14598, #11424, #16756 ) ) ;
#11876=DIRECTION ( 'NONE',  ( 0.000000000000000000, 0.000000000000000000, 1.000000000000000000 ) ) ;
#11923=AXIS2_PLACEMENT_3D ( 'NONE', #14516, #9109, #10828 ) ;
#11941=EDGE_CURVE ( 'NONE', #15487, #5457, #9820, .T. ) ;
#11980=CARTESIAN_POINT ( 'NONE',  ( 0.000000000000000000, 38.00000000000000711, -5.741599279633704455E-16 ) ) ;
#12030=EDGE_CURVE ( 'NONE', #8474, #4609, #15125, .T. ) ;
#12048=EDGE_CURVE ( 'NONE', #16344, #12347, #14366, .T. ) ;
#12071=DIRECTION ( 'NONE',  ( 1.000000000000000000, 0.000000000000000000, 0.000000000000000000 ) ) ;
#12072=DIRECTION ( 'NONE',  ( 1.000000000000000000, 0.000000000000000000, 0.000000000000000000 ) ) ;
#12100=CARTESIAN_POINT ( 'NONE',  ( -7.005190481990339112E-15, 37.39913938097243573, -5.741599279633704455E-16 ) ) ;
#12103=B_SPLINE_CURVE_WITH_KNOTS ( 'NONE', 3,
 ( #812, #8455, #11272, #9669, #1919, #3385, #6028, #5955, #12401, #15143, #11197, #6989, #4424, #3300, #560, #16430, #13861, #480 ),
 .UNSPECIFIED., .F., .F.,
 ( 4, 2, 2, 2, 2, 2, 2, 2, 4 ),
 ( 0.004721323624227206743, 0.005310725018217476653, 0.005900126412207745696, 0.006489527806198015607, 0.007078929200188285517, 0.007668330594178554560, 0.008257731988168825338, 0.008847133382159092646, 0.009436534776149363424 ),
 .UNSPECIFIED. ) ;
#12153=EDGE_CURVE ( 'NONE', #9431, #11779, #9159, .T. ) ;
#12227=DIRECTION ( 'NONE',  ( -0.000000000000000000, 1.000000000000000000, -0.000000000000000000 ) ) ;
#12304=DIRECTION ( 'NONE',  ( 0.000000000000000000, 0.000000000000000000, -1.000000000000000000 ) ) ;
#12309=ORIENTED_EDGE ( 'NONE', *, *, #12153, .F. ) ;
#12332=CARTESIAN_POINT ( 'NONE',  ( -3.000000000000002220, 60.00000000000000711, 6.000000000000000000 ) ) ;
#12347=VERTEX_POINT ( 'NONE', #16321 ) ;
#12401=CARTESIAN_POINT ( 'NONE',  ( -1.983673311716146026, 38.74097077230339892, 9.291669371308643122 ) ) ;
#12420=CARTESIAN_POINT ( 'NONE',  ( 2.257948793614858118, 39.01519438325225053, 9.228844315538687226 ) ) ;
#12470=DIRECTION ( 'NONE',  ( 0.000000000000000000, 0.000000000000000000, 1.000000000000000000 ) ) ;
#12486=ORIENTED_EDGE ( 'NONE', *, *, #13504, .T. ) ;
#12494=DIRECTION ( 'NONE',  ( 0.000000000000000000, 1.000000000000000000, 0.000000000000000000 ) ) ;
#12559=ORIENTED_EDGE ( 'NONE', *, *, #7612, .F. ) ;
#12563=ORIENTED_EDGE ( 'NONE', *, *, #2144, .F. ) ;
#12615=LINE ( 'NONE', #11327, #8742 ) ;
#12640=CARTESIAN_POINT ( 'NONE',  ( 0.000000000000000000, 38.00000000000000711, -5.741599279633704455E-16 ) ) ;
#12732=ORIENTED_EDGE ( 'NONE', *, *, #7286, .F. ) ;
#12768=EDGE_CURVE ( 'NONE', #7178, #5457, #15001, .T. ) ;
#12846=ORIENTED_EDGE ( 'NONE', *, *, #15354, .T. ) ;
#12860=EDGE_CURVE ( 'NONE', #985, #8625, #9785, .T. ) ;
#12902=ORIENTED_EDGE ( 'NONE', *, *, #16907, .F. ) ;
#12930=CLOSED_SHELL ( 'NONE', ( #11736, #9314, #2793, #1314, #15977, #10141, #9760, #975, #7416, #13868, #16100, #10963, #45, #1633, #2995, #10702, #3785, #5184 ) ) ;
#13037=DIRECTION ( 'NONE',  ( 0.000000000000000000, 1.000000000000000000, 0.000000000000000000 ) ) ;
#13081=VECTOR ( 'NONE', #13199, 1000.000000000000000 ) ;
#13199=DIRECTION ( 'NONE',  ( 8.659560562354968603E-17, 0.7071067811865445751, -0.7071067811865504593 ) ) ;
#13220=DIRECTION ( 'NONE',  ( 0.000000000000000000, 0.5150380749100629263, 0.8571673007021070045 ) ) ;
#13224=AXIS2_PLACEMENT_3D ( 'NONE', #4451, #16213, #5390 ) ;
#13243=APPLICATION_CONTEXT ( 'automotive_design' ) ;
#13267=DIRECTION ( 'NONE',  ( 0.000000000000000000, -0.000000000000000000, 1.000000000000000000 ) ) ;
#13278=VECTOR ( 'NONE', #6736, 1000.000000000000000 ) ;
#13348=CARTESIAN_POINT ( 'NONE',  ( 0.000000000000000000, 38.00000000000000711, -5.741599279633704455E-16 ) ) ;
#13396=CARTESIAN_POINT ( 'NONE',  ( 2.999999999999996891, 60.00000000000000711, 6.000000000000000000 ) ) ;
#13410=ORIENTED_EDGE ( 'NONE', *, *, #11941, .T. ) ;
#13418=EDGE_CURVE ( 'NONE', #5457, #8068, #8231, .T. ) ;
#13453=DIRECTION ( 'NONE',  ( 0.000000000000000000, 1.000000000000000000, 0.000000000000000000 ) ) ;
#13468=CARTESIAN_POINT ( 'NONE',  ( 2.903217335657448661, 40.21902629923274475, 9.045605051663343943 ) ) ;
#13504=EDGE_CURVE ( 'NONE', #8747, #8625, #10687, .T. ) ;
#13568=DIRECTION ( 'NONE',  ( -0.000000000000000000, -0.000000000000000000, 1.000000000000000000 ) ) ;
#13590=( NAMED_UNIT ( * ) PLANE_ANGLE_UNIT ( ) SI_UNIT ( $, .RADIAN. ) );
#13600=CARTESIAN_POINT ( 'NONE',  ( 2.600106608147765286, 61.50910620841189314, 9.137947797636652325 ) ) ;
#13626=DIRECTION ( 'NONE',  ( -0.000000000000000000, -0.000000000000000000, 1.000000000000000000 ) ) ;
#13630=AXIS2_PLACEMENT_3D ( 'NONE', #1356, #15362, #8837 ) ;
#13642=VECTOR ( 'NONE', #13568, 1000.000000000000000 ) ;
#13662=LINE ( 'NONE', #604, #5827 ) ;
#13678=CARTESIAN_POINT ( 'NONE',  ( 2.844582250340499385, 60.97290968073905759, 9.064464814046607088 ) ) ;
#13689=CARTESIAN_POINT ( 'NONE',  ( 1.224646799147349016E-16, 66.00000000000000000, -0.9999999999999972244 ) ) ;
#13720=EDGE_CURVE ( 'NONE', #11801, #7178, #3508, .T. ) ;
#13736=AXIS2_PLACEMENT_3D ( 'NONE', #10601, #4077, #8011 ) ;
#13788=DIRECTION ( 'NONE',  ( 1.141265444721583757E-16, -1.000000000000000000, 0.000000000000000000 ) ) ;
#13807=EDGE_CURVE ( 'NONE', #4810, #985, #9869, .T. ) ;
#13826=AXIS2_PLACEMENT_3D ( 'NONE', #6813, #8283, #12071 ) ;
#13836=SURFACE_SIDE_STYLE ('',( #7292 ) ) ;
#13838=ORIENTED_EDGE ( 'NONE', *, *, #13418, .F. ) ;
#13847=CARTESIAN_POINT ( 'NONE',  ( -1.224646799147350495E-16, 41.00000000000000711, 6.000000000000000000 ) ) ;
#13848=FACE_OUTER_BOUND ( 'NONE', #5279, .T. ) ;
#13861=CARTESIAN_POINT ( 'NONE',  ( -3.000000000000001776, 40.80057950988138771, 9.013878188659973034 ) ) ;
#13868=ADVANCED_FACE ( 'NONE', ( #2635, #15355 ), #4950, .T. ) ;
#13883=PLANE ( 'NONE',  #9081 ) ;
#13928=CARTESIAN_POINT ( 'NONE',  ( 1.507804506096818820, 62.60084458484482894, 9.381017998102993971 ) ) ;
#13955=CARTESIAN_POINT ( 'NONE',  ( 0.000000000000000000, 66.00000000000000000, 0.000000000000000000 ) ) ;
#13975=CARTESIAN_POINT ( 'NONE',  ( -3.000000000000002220, 60.19966235751221006, 9.013878188659974811 ) ) ;
#14009=DIRECTION ( 'NONE',  ( -0.000000000000000000, -0.000000000000000000, 1.000000000000000000 ) ) ;
#14010=DIRECTION ( 'NONE',  ( -0.000000000000000000, 1.000000000000000000, -0.000000000000000000 ) ) ;
#14033=CARTESIAN_POINT ( 'NONE',  ( 3.000000000000000000, 41.00000000000000711, 6.000000000000000000 ) ) ;
#14043=ORIENTED_EDGE ( 'NONE', *, *, #13807, .T. ) ;
#14053=ORIENTED_EDGE ( 'NONE', *, *, #12860, .T. ) ;
#14162=CARTESIAN_POINT ( 'NONE',  ( -1.224646799147350495E-16, 41.00000000000000711, 6.000000000000000000 ) ) ;
#14266=CARTESIAN_POINT ( 'NONE',  ( 1.163414459189985485E-15, 66.00000000000000000, 9.500000000000000000 ) ) ;
#14271=EDGE_CURVE ( 'NONE', #214, #11801, #12103, .T. ) ;
#14304=CARTESIAN_POINT ( 'NONE',  ( 0.000000000000000000, 66.00000000000000000, 1.799999999999999600 ) ) ;
#14344=VECTOR ( 'NONE', #11501, 1000.000000000000000 ) ;
#14350=DIRECTION ( 'NONE',  ( 0.000000000000000000, 0.000000000000000000, 1.000000000000000000 ) ) ;
#14353=ORIENTED_EDGE ( 'NONE', *, *, #16214, .T. ) ;
#14366=CIRCLE ( 'NONE', #9985, 12.00000000000000178 ) ;
#14376=AXIS2_PLACEMENT_3D ( 'NONE', #12332, #3061, #13788 ) ;
#14474=CARTESIAN_POINT ( 'NONE',  ( 0.000000000000000000, 10.00000000000000000, 0.000000000000000000 ) ) ;
#14516=CARTESIAN_POINT ( 'NONE',  ( 0.000000000000000000, 10.00000000000000000, 0.000000000000000000 ) ) ;
#14555=CARTESIAN_POINT ( 'NONE',  ( 1.163414457778310218E-15, 63.00000000000000000, 9.500000000000000000 ) ) ;
#14592=FACE_OUTER_BOUND ( 'NONE', #1175, .T. ) ;
#14598=ORIENTED_EDGE ( 'NONE', *, *, #1726, .T. ) ;
#14626=LINE ( 'NONE', #15994, #4478 ) ;
#14642=DIRECTION ( 'NONE',  ( 0.000000000000000000, 0.000000000000000000, 1.000000000000000000 ) ) ;
#14646=B_SPLINE_CURVE_WITH_KNOTS ( 'NONE', 3,
 ( #10705, #16036, #10537, #13468, #4604, #5641, #10964, #5891, #12420, #497, #16200, #8647, #8398, #14835, #16371, #7337 ),
 .UNSPECIFIED., .F., .F.,
 ( 4, 2, 2, 2, 2, 2, 2, 4 ),
 ( 0.000000000000000000, 0.0005901654530283999755, 0.001180330906056799951, 0.001770496359085199818, 0.002360661812113599902, 0.003540992718170399636, 0.004131158171198803623, 0.004721323624227206743 ),
 .UNSPECIFIED. ) ;
#14663=CARTESIAN_POINT ( 'NONE',  ( 2.204364238465236069E-16, 66.00000000000000000, -1.800000000000000711 ) ) ;
#14669=ORIENTED_EDGE ( 'NONE', *, *, #12048, .T. ) ;
#14689=DIRECTION ( 'NONE',  ( 0.000000000000000000, 0.000000000000000000, -1.000000000000000000 ) ) ;
#14703=VECTOR ( 'NONE', #1216, 1000.000000000000000 ) ;
#14704=CIRCLE ( 'NONE', #9782, 12.00000000000000178 ) ;
#14782=CYLINDRICAL_SURFACE ( 'NONE', #893, 0.9999999999999965583 ) ;
#14796=EDGE_CURVE ( 'NONE', #8672, #11572, #3100, .T. ) ;
#14835=CARTESIAN_POINT ( 'NONE',  ( 0.3928280596732524055, 38.01925660030116205, 9.493865254640489582 ) ) ;
#14873=ORIENTED_EDGE ( 'NONE', *, *, #1726, .F. ) ;
#14894=AXIS2_PLACEMENT_3D ( 'NONE', #14162, #5037, #10456 ) ;
#14916=ORIENTED_EDGE ( 'NONE', *, *, #13418, .T. ) ;
#14933=CARTESIAN_POINT ( 'NONE',  ( -0.3928280596732490748, 62.98074339969887347, 9.493865254640493134 ) ) ;
#15001=B_SPLINE_CURVE_WITH_KNOTS ( 'NONE', 3,
 ( #11146, #13975, #7017, #2116, #1949, #16383, #3251, #15015, #15090, #9946, #8658, #840, #3500, #14933, #7172, #11226 ),
 .UNSPECIFIED., .F., .F.,
 ( 4, 2, 2, 2, 2, 2, 2, 4 ),
 ( 0.000000000000000000, 0.0005901654530283981324, 0.001180330906056796265, 0.001770496359085194180, 0.002360661812113592530, 0.003540992718170401805, 0.004131158171198806225, 0.004721323624227211080 ),
 .UNSPECIFIED. ) ;
#15015=CARTESIAN_POINT ( 'NONE',  ( -2.383743612111324239, 61.83195493428745237, 9.196765735797573171 ) ) ;
#15046=CARTESIAN_POINT ( 'NONE',  ( 1.163414459189985485E-15, 66.00000000000000000, 9.500000000000000000 ) ) ;
#15078=ORIENTED_EDGE ( 'NONE', *, *, #13720, .F. ) ;
#15090=CARTESIAN_POINT ( 'NONE',  ( -2.257948793614859451, 61.98480561674775657, 9.228844315538689003 ) ) ;
#15122=DIRECTION ( 'NONE',  ( -0.000000000000000000, -1.000000000000000000, -0.000000000000000000 ) ) ;
#15125=LINE ( 'NONE', #11260, #16284 ) ;
#15143=CARTESIAN_POINT ( 'NONE',  ( -2.259918635623970218, 39.01734001413205277, 9.228371864727252571 ) ) ;
#15172=DIRECTION ( 'NONE',  ( 0.000000000000000000, 1.000000000000000000, 0.000000000000000000 ) ) ;
#15204=VECTOR ( 'NONE', #11737, 1000.000000000000000 ) ;
#15217=DIRECTION ( 'NONE',  ( 1.000000000000000000, 0.000000000000000000, 0.000000000000000000 ) ) ;
#15274=DIRECTION ( 'NONE',  ( 0.000000000000000000, 0.000000000000000000, 1.000000000000000000 ) ) ;
#15305=FACE_OUTER_BOUND ( 'NONE', #2499, .T. ) ;
#15326=CARTESIAN_POINT ( 'NONE',  ( 1.163414457778310218E-15, 63.00000000000000000, 9.500000000000000000 ) ) ;
#15345=EDGE_LOOP ( 'NONE', ( #2943, #1274, #7453 ) ) ;
#15354=EDGE_CURVE ( 'NONE', #11419, #7051, #5577, .T. ) ;
#15355=FACE_OUTER_BOUND ( 'NONE', #3572, .T. ) ;
#15362=DIRECTION ( 'NONE',  ( -0.000000000000000000, 1.000000000000000000, -0.000000000000000000 ) ) ;
#15380=EDGE_LOOP ( 'NONE', ( #12732, #11181, #2716, #15484 ) ) ;
#15389=CARTESIAN_POINT ( 'NONE',  ( 2.999999999999996891, 60.00000000000000711, 6.000000000000000000 ) ) ;
#15396=EDGE_CURVE ( 'NONE', #6601, #16595, #16014, .T. ) ;
#15461=AXIS2_PLACEMENT_3D ( 'NONE', #12640, #7388, #9901 ) ;
#15484=ORIENTED_EDGE ( 'NONE', *, *, #11099, .F. ) ;
#15487=VERTEX_POINT ( 'NONE', #892 ) ;
#15561=PLANE ( 'NONE',  #1202 ) ;
#15630=CARTESIAN_POINT ( 'NONE',  ( 1.469576158976824144E-15, 0.000000000000000000, 12.00000000000000178 ) ) ;
#15632=DIRECTION ( 'NONE',  ( 0.000000000000000000, 1.000000000000000000, 0.000000000000000000 ) ) ;
#15735=( GEOMETRIC_REPRESENTATION_CONTEXT ( 3 ) GLOBAL_UNCERTAINTY_ASSIGNED_CONTEXT ( ( #9626 ) ) GLOBAL_UNIT_ASSIGNED_CONTEXT ( ( #9724, #13590, #16238 ) ) REPRESENTATION_CONTEXT ( 'NONE', 'WORKASPACE' ) );
#15770=EDGE_LOOP ( 'NONE', ( #8432, #7731, #11293, #6689 ) ) ;
#15827=EDGE_CURVE ( 'NONE', #4810, #4609, #5316, .T. ) ;
#15847=LINE ( 'NONE', #9410, #13278 ) ;
#15877=ORIENTED_EDGE ( 'NONE', *, *, #15827, .F. ) ;
#15887=VERTEX_POINT ( 'NONE', #1903 ) ;
#15903=CARTESIAN_POINT ( 'NONE',  ( 0.000000000000000000, 0.000000000000000000, -12.00000000000000178 ) ) ;
#15977=ADVANCED_FACE ( 'NONE', ( #13848 ), #11257, .T. ) ;
#15991=DIRECTION ( 'NONE',  ( 0.000000000000000000, 0.000000000000000000, 1.000000000000000000 ) ) ;
#15994=CARTESIAN_POINT ( 'NONE',  ( 1.469576158976824144E-15, 10.00000000000000000, 12.00000000000000178 ) ) ;
#15996=EDGE_LOOP ( 'NONE', ( #2760, #2674, #8354, #14353, #11581, #5832, #8421, #3912 ) ) ;
#16002=CARTESIAN_POINT ( 'NONE',  ( 0.000000000000000000, 65.20000000000000284, 0.9999999999999976685 ) ) ;
#16014=CIRCLE ( 'NONE', #2022, 9.500000000000000000 ) ;
#16015=DIRECTION ( 'NONE',  ( 0.000000000000000000, 0.000000000000000000, -1.000000000000000000 ) ) ;
#16017=FACE_OUTER_BOUND ( 'NONE', #2453, .T. ) ;
#16027=LINE ( 'NONE', #14663, #13081 ) ;
#16034=ORIENTED_EDGE ( 'NONE', *, *, #12860, .F. ) ;
#16036=CARTESIAN_POINT ( 'NONE',  ( 3.000000000000000888, 40.80033764248782546, 9.013878188659974811 ) ) ;
#16077=ORIENTED_EDGE ( 'NONE', *, *, #10215, .F. ) ;
#16094=VECTOR ( 'NONE', #9696, 1000.000000000000000 ) ;
#16100=ADVANCED_FACE ( 'NONE', ( #15305 ), #16837, .F. ) ;
#16137=CYLINDRICAL_SURFACE ( 'NONE', #3618, 9.500000000000000000 ) ;
#16168=VECTOR ( 'NONE', #5987, 1000.000000000000000 ) ;
#16200=CARTESIAN_POINT ( 'NONE',  ( 1.512611822017149166, 38.37995103523728346, 9.385845453595075938 ) ) ;
#16213=DIRECTION ( 'NONE',  ( -0.000000000000000000, 1.000000000000000000, -0.000000000000000000 ) ) ;
#16214=EDGE_CURVE ( 'NONE', #16595, #6601, #953, .T. ) ;
#16238=( NAMED_UNIT ( * ) SI_UNIT ( $, .STERADIAN. ) SOLID_ANGLE_UNIT ( ) );
#16284=VECTOR ( 'NONE', #4727, 1000.000000000000114 ) ;
#16304=CYLINDRICAL_SURFACE ( 'NONE', #7300, 9.500000000000000000 ) ;
#16321=CARTESIAN_POINT ( 'NONE',  ( 1.469576158976824144E-15, 10.00000000000000000, 12.00000000000000178 ) ) ;
#16344=VERTEX_POINT ( 'NONE', #2282 ) ;
#16356=DIRECTION ( 'NONE',  ( 0.000000000000000000, 0.000000000000000000, 1.000000000000000000 ) ) ;
#16371=CARTESIAN_POINT ( 'NONE',  ( 0.1972064085032624869, 38.00000000000002132, 9.500000000000005329 ) ) ;
#16383=CARTESIAN_POINT ( 'NONE',  ( -2.693790225569811625, 61.33495048777871261, 9.110418847747206783 ) ) ;
#16430=CARTESIAN_POINT ( 'NONE',  ( -2.979937318121947509, 40.60126023706489917, 9.020623939867236984 ) ) ;
#16450=DIRECTION ( 'NONE',  ( 0.000000000000000000, 0.000000000000000000, 1.000000000000000000 ) ) ;
#16488=CARTESIAN_POINT ( 'NONE',  ( 2.979937318121946177, 60.39873976293512214, 9.020623939867238761 ) ) ;
#16532=ORIENTED_EDGE ( 'NONE', *, *, #1086, .F. ) ;
#16554=EDGE_LOOP ( 'NONE', ( #7919, #7773, #6630, #8652 ) ) ;
#16595=VERTEX_POINT ( 'NONE', #3916 ) ;
#16639=EDGE_CURVE ( 'NONE', #7051, #7178, #15847, .T. ) ;
#16668=DIRECTION ( 'NONE',  ( -0.000000000000000000, -1.000000000000000000, -0.000000000000000000 ) ) ;
#16715=DIRECTION ( 'NONE',  ( 0.000000000000000000, 1.000000000000000000, 0.000000000000000000 ) ) ;
#16756=ORIENTED_EDGE ( 'NONE', *, *, #3706, .T. ) ;
#16837=CONICAL_SURFACE ( 'NONE', #8362, 0.9999999999999950040, 1.029744258676644320 ) ;
#16847=PRODUCT ( 'Servo-Axe', 'Servo-Axe', '', ( #3277 ) ) ;
#16860=CARTESIAN_POINT ( 'NONE',  ( 3.000000000000000000, 41.00000000000000711, 9.013878188659973034 ) ) ;
#16907=EDGE_CURVE ( 'NONE', #15487, #15887, #8603, .T. ) ;
ENDSEC;
END-ISO-10303-21;
